ISO-10303-21;
HEADER;
/* Generated by software containing ST-Developer
 * from STEP Tools, Inc. (www.steptools.com) 
 */

FILE_DESCRIPTION(
/* description */ ('Chain-less indexing wheel (Geneva) drive'),
/* implementation_level */ '2;1');

FILE_NAME(
/* name */ 'Cap Screw - M5x20.step',
/* time_stamp */ '2026-10-28T03:25:22-07:00',
/* author */ (''),
/* organization */ (''),
/* preprocessor_version */ 'ST-DEVELOPER v20.2',
/* originating_system */ 'Autodesk Translation Framework v15.17.0.0',
/* authorisation */ '');

FILE_SCHEMA (('AUTOMOTIVE_DESIGN { 1 0 10303 214 3 1 1 }'));
ENDSEC;

DATA;
#10=MECHANICAL_DESIGN_GEOMETRIC_PRESENTATION_REPRESENTATION('',(#309),#10957);
#197=ORIENTED_CLOSED_SHELL('',*,#5706,.F.);
#199=CONICAL_SURFACE('',#6247,0.4,0.785398163397448);
#200=CONICAL_SURFACE('',#6251,0.41,0.785398163397448);
#201=CONICAL_SURFACE('',#6255,0.26,0.463647609000806);
#202=CONICAL_SURFACE('',#6259,0.225,0.785398163397448);
#211=BREP_WITH_VOIDS('Body1',#5705,(#197));
#259=SHAPE_REPRESENTATION_RELATIONSHIP('SRR','None',#11072,#284);
#284=ADVANCED_BREP_SHAPE_REPRESENTATION('',(#211),#10935);
#309=STYLED_ITEM('',(#11294),#211);
#423=FACE_BOUND('',#1154,.T.);
#528=PLANE('',#6245);
#529=PLANE('',#6253);
#530=PLANE('',#6261);
#531=PLANE('',#6262);
#532=PLANE('',#6263);
#533=PLANE('',#6264);
#534=PLANE('',#6265);
#535=PLANE('',#6266);
#536=PLANE('',#6267);
#537=PLANE('',#6268);
#538=PLANE('',#6269);
#760=FACE_OUTER_BOUND('',#1149,.T.);
#761=FACE_OUTER_BOUND('',#1150,.T.);
#762=FACE_OUTER_BOUND('',#1151,.T.);
#763=FACE_OUTER_BOUND('',#1152,.T.);
#764=FACE_OUTER_BOUND('',#1153,.T.);
#765=FACE_OUTER_BOUND('',#1155,.T.);
#766=FACE_OUTER_BOUND('',#1156,.T.);
#767=FACE_OUTER_BOUND('',#1157,.T.);
#768=FACE_OUTER_BOUND('',#1158,.T.);
#769=FACE_OUTER_BOUND('',#1159,.T.);
#770=FACE_OUTER_BOUND('',#1160,.T.);
#771=FACE_OUTER_BOUND('',#1161,.T.);
#772=FACE_OUTER_BOUND('',#1162,.T.);
#773=FACE_OUTER_BOUND('',#1163,.T.);
#774=FACE_OUTER_BOUND('',#1164,.T.);
#775=FACE_OUTER_BOUND('',#1165,.T.);
#776=FACE_OUTER_BOUND('',#1166,.T.);
#1149=EDGE_LOOP('',(#4235));
#1150=EDGE_LOOP('',(#4236,#4237,#4238,#4239));
#1151=EDGE_LOOP('',(#4240,#4241,#4242,#4243));
#1152=EDGE_LOOP('',(#4244,#4245,#4246,#4247));
#1153=EDGE_LOOP('',(#4248));
#1154=EDGE_LOOP('',(#4249));
#1155=EDGE_LOOP('',(#4250,#4251,#4252,#4253));
#1156=EDGE_LOOP('',(#4254,#4255,#4256,#4257));
#1157=EDGE_LOOP('',(#4258,#4259,#4260,#4261));
#1158=EDGE_LOOP('',(#4262));
#1159=EDGE_LOOP('',(#4263,#4264,#4265,#4266));
#1160=EDGE_LOOP('',(#4267,#4268,#4269,#4270));
#1161=EDGE_LOOP('',(#4271,#4272,#4273,#4274));
#1162=EDGE_LOOP('',(#4275,#4276,#4277,#4278));
#1163=EDGE_LOOP('',(#4279,#4280,#4281,#4282));
#1164=EDGE_LOOP('',(#4283,#4284,#4285,#4286));
#1165=EDGE_LOOP('',(#4287,#4288,#4289,#4290,#4291,#4292));
#1166=EDGE_LOOP('',(#4293,#4294,#4295,#4296,#4297,#4298));
#1547=LINE('',#9186,#1921);
#1548=LINE('',#9190,#1922);
#1549=LINE('',#9194,#1923);
#1550=LINE('',#9201,#1924);
#1551=LINE('',#9205,#1925);
#1552=LINE('',#9209,#1926);
#1553=LINE('',#9214,#1927);
#1554=LINE('',#9216,#1928);
#1555=LINE('',#9218,#1929);
#1556=LINE('',#9219,#1930);
#1557=LINE('',#9222,#1931);
#1558=LINE('',#9224,#1932);
#1559=LINE('',#9225,#1933);
#1560=LINE('',#9228,#1934);
#1561=LINE('',#9230,#1935);
#1562=LINE('',#9231,#1936);
#1563=LINE('',#9234,#1937);
#1564=LINE('',#9236,#1938);
#1565=LINE('',#9237,#1939);
#1566=LINE('',#9240,#1940);
#1567=LINE('',#9242,#1941);
#1568=LINE('',#9243,#1942);
#1569=LINE('',#9245,#1943);
#1570=LINE('',#9246,#1944);
#1921=VECTOR('',#7351,0.4);
#1922=VECTOR('',#7356,0.425);
#1923=VECTOR('',#7361,0.41);
#1924=VECTOR('',#7370,0.26);
#1925=VECTOR('',#7375,0.25);
#1926=VECTOR('',#7380,0.225);
#1927=VECTOR('',#7385,1.);
#1928=VECTOR('',#7386,1.);
#1929=VECTOR('',#7387,1.);
#1930=VECTOR('',#7388,1.);
#1931=VECTOR('',#7391,1.);
#1932=VECTOR('',#7392,1.);
#1933=VECTOR('',#7393,1.);
#1934=VECTOR('',#7396,1.);
#1935=VECTOR('',#7397,1.);
#1936=VECTOR('',#7398,1.);
#1937=VECTOR('',#7401,1.);
#1938=VECTOR('',#7402,1.);
#1939=VECTOR('',#7403,1.);
#1940=VECTOR('',#7406,1.);
#1941=VECTOR('',#7407,1.);
#1942=VECTOR('',#7408,1.);
#1943=VECTOR('',#7411,1.);
#1944=VECTOR('',#7412,1.);
#2289=CIRCLE('',#6246,0.375);
#2290=CIRCLE('',#6248,0.425);
#2291=CIRCLE('',#6250,0.425);
#2292=CIRCLE('',#6252,0.395);
#2293=CIRCLE('',#6254,0.27);
#2294=CIRCLE('',#6256,0.24505);
#2295=CIRCLE('',#6258,0.24505);
#2296=CIRCLE('',#6260,0.2);
#2657=VERTEX_POINT('',#9181);
#2658=VERTEX_POINT('',#9184);
#2659=VERTEX_POINT('',#9188);
#2660=VERTEX_POINT('',#9192);
#2661=VERTEX_POINT('',#9196);
#2662=VERTEX_POINT('',#9199);
#2663=VERTEX_POINT('',#9203);
#2664=VERTEX_POINT('',#9207);
#2665=VERTEX_POINT('',#9212);
#2666=VERTEX_POINT('',#9213);
#2667=VERTEX_POINT('',#9215);
#2668=VERTEX_POINT('',#9217);
#2669=VERTEX_POINT('',#9221);
#2670=VERTEX_POINT('',#9223);
#2671=VERTEX_POINT('',#9227);
#2672=VERTEX_POINT('',#9229);
#2673=VERTEX_POINT('',#9233);
#2674=VERTEX_POINT('',#9235);
#2675=VERTEX_POINT('',#9239);
#2676=VERTEX_POINT('',#9241);
#3243=EDGE_CURVE('',#2657,#2657,#2289,.T.);
#3244=EDGE_CURVE('',#2658,#2658,#2290,.T.);
#3245=EDGE_CURVE('',#2658,#2657,#1547,.T.);
#3246=EDGE_CURVE('',#2659,#2659,#2291,.T.);
#3247=EDGE_CURVE('',#2659,#2658,#1548,.T.);
#3248=EDGE_CURVE('',#2660,#2660,#2292,.T.);
#3249=EDGE_CURVE('',#2660,#2659,#1549,.T.);
#3250=EDGE_CURVE('',#2661,#2661,#2293,.T.);
#3251=EDGE_CURVE('',#2662,#2662,#2294,.F.);
#3252=EDGE_CURVE('',#2662,#2661,#1550,.T.);
#3253=EDGE_CURVE('',#2663,#2663,#2295,.F.);
#3254=EDGE_CURVE('',#2663,#2662,#1551,.T.);
#3255=EDGE_CURVE('',#2664,#2664,#2296,.T.);
#3256=EDGE_CURVE('',#2664,#2663,#1552,.T.);
#3257=EDGE_CURVE('',#2665,#2666,#1553,.T.);
#3258=EDGE_CURVE('',#2666,#2667,#1554,.T.);
#3259=EDGE_CURVE('',#2667,#2668,#1555,.T.);
#3260=EDGE_CURVE('',#2665,#2668,#1556,.T.);
#3261=EDGE_CURVE('',#2666,#2669,#1557,.T.);
#3262=EDGE_CURVE('',#2669,#2670,#1558,.T.);
#3263=EDGE_CURVE('',#2670,#2667,#1559,.T.);
#3264=EDGE_CURVE('',#2669,#2671,#1560,.T.);
#3265=EDGE_CURVE('',#2671,#2672,#1561,.T.);
#3266=EDGE_CURVE('',#2672,#2670,#1562,.T.);
#3267=EDGE_CURVE('',#2671,#2673,#1563,.T.);
#3268=EDGE_CURVE('',#2673,#2674,#1564,.T.);
#3269=EDGE_CURVE('',#2674,#2672,#1565,.T.);
#3270=EDGE_CURVE('',#2673,#2675,#1566,.T.);
#3271=EDGE_CURVE('',#2675,#2676,#1567,.T.);
#3272=EDGE_CURVE('',#2676,#2674,#1568,.T.);
#3273=EDGE_CURVE('',#2675,#2665,#1569,.T.);
#3274=EDGE_CURVE('',#2668,#2676,#1570,.T.);
#4235=ORIENTED_EDGE('',*,*,#3243,.F.);
#4236=ORIENTED_EDGE('',*,*,#3244,.F.);
#4237=ORIENTED_EDGE('',*,*,#3245,.T.);
#4238=ORIENTED_EDGE('',*,*,#3243,.T.);
#4239=ORIENTED_EDGE('',*,*,#3245,.F.);
#4240=ORIENTED_EDGE('',*,*,#3246,.F.);
#4241=ORIENTED_EDGE('',*,*,#3247,.T.);
#4242=ORIENTED_EDGE('',*,*,#3244,.T.);
#4243=ORIENTED_EDGE('',*,*,#3247,.F.);
#4244=ORIENTED_EDGE('',*,*,#3248,.F.);
#4245=ORIENTED_EDGE('',*,*,#3249,.T.);
#4246=ORIENTED_EDGE('',*,*,#3246,.T.);
#4247=ORIENTED_EDGE('',*,*,#3249,.F.);
#4248=ORIENTED_EDGE('',*,*,#3248,.T.);
#4249=ORIENTED_EDGE('',*,*,#3250,.F.);
#4250=ORIENTED_EDGE('',*,*,#3251,.F.);
#4251=ORIENTED_EDGE('',*,*,#3252,.T.);
#4252=ORIENTED_EDGE('',*,*,#3250,.T.);
#4253=ORIENTED_EDGE('',*,*,#3252,.F.);
#4254=ORIENTED_EDGE('',*,*,#3253,.F.);
#4255=ORIENTED_EDGE('',*,*,#3254,.T.);
#4256=ORIENTED_EDGE('',*,*,#3251,.T.);
#4257=ORIENTED_EDGE('',*,*,#3254,.F.);
#4258=ORIENTED_EDGE('',*,*,#3255,.F.);
#4259=ORIENTED_EDGE('',*,*,#3256,.T.);
#4260=ORIENTED_EDGE('',*,*,#3253,.T.);
#4261=ORIENTED_EDGE('',*,*,#3256,.F.);
#4262=ORIENTED_EDGE('',*,*,#3255,.T.);
#4263=ORIENTED_EDGE('',*,*,#3257,.T.);
#4264=ORIENTED_EDGE('',*,*,#3258,.T.);
#4265=ORIENTED_EDGE('',*,*,#3259,.T.);
#4266=ORIENTED_EDGE('',*,*,#3260,.F.);
#4267=ORIENTED_EDGE('',*,*,#3261,.T.);
#4268=ORIENTED_EDGE('',*,*,#3262,.T.);
#4269=ORIENTED_EDGE('',*,*,#3263,.T.);
#4270=ORIENTED_EDGE('',*,*,#3258,.F.);
#4271=ORIENTED_EDGE('',*,*,#3264,.T.);
#4272=ORIENTED_EDGE('',*,*,#3265,.T.);
#4273=ORIENTED_EDGE('',*,*,#3266,.T.);
#4274=ORIENTED_EDGE('',*,*,#3262,.F.);
#4275=ORIENTED_EDGE('',*,*,#3267,.T.);
#4276=ORIENTED_EDGE('',*,*,#3268,.T.);
#4277=ORIENTED_EDGE('',*,*,#3269,.T.);
#4278=ORIENTED_EDGE('',*,*,#3265,.F.);
#4279=ORIENTED_EDGE('',*,*,#3270,.T.);
#4280=ORIENTED_EDGE('',*,*,#3271,.T.);
#4281=ORIENTED_EDGE('',*,*,#3272,.T.);
#4282=ORIENTED_EDGE('',*,*,#3268,.F.);
#4283=ORIENTED_EDGE('',*,*,#3273,.T.);
#4284=ORIENTED_EDGE('',*,*,#3260,.T.);
#4285=ORIENTED_EDGE('',*,*,#3274,.T.);
#4286=ORIENTED_EDGE('',*,*,#3271,.F.);
#4287=ORIENTED_EDGE('',*,*,#3273,.F.);
#4288=ORIENTED_EDGE('',*,*,#3270,.F.);
#4289=ORIENTED_EDGE('',*,*,#3267,.F.);
#4290=ORIENTED_EDGE('',*,*,#3264,.F.);
#4291=ORIENTED_EDGE('',*,*,#3261,.F.);
#4292=ORIENTED_EDGE('',*,*,#3257,.F.);
#4293=ORIENTED_EDGE('',*,*,#3274,.F.);
#4294=ORIENTED_EDGE('',*,*,#3259,.F.);
#4295=ORIENTED_EDGE('',*,*,#3263,.F.);
#4296=ORIENTED_EDGE('',*,*,#3266,.F.);
#4297=ORIENTED_EDGE('',*,*,#3269,.F.);
#4298=ORIENTED_EDGE('',*,*,#3272,.F.);
#5295=CYLINDRICAL_SURFACE('',#6249,0.425);
#5296=CYLINDRICAL_SURFACE('',#6257,0.24505);
#5474=ADVANCED_FACE('',(#760),#528,.T.);
#5475=ADVANCED_FACE('',(#761),#199,.T.);
#5476=ADVANCED_FACE('',(#762),#5295,.T.);
#5477=ADVANCED_FACE('',(#763),#200,.T.);
#5478=ADVANCED_FACE('',(#764,#423),#529,.T.);
#5479=ADVANCED_FACE('',(#765),#201,.T.);
#5480=ADVANCED_FACE('',(#766),#5296,.T.);
#5481=ADVANCED_FACE('',(#767),#202,.T.);
#5482=ADVANCED_FACE('',(#768),#530,.T.);
#5483=ADVANCED_FACE('',(#769),#531,.F.);
#5484=ADVANCED_FACE('',(#770),#532,.F.);
#5485=ADVANCED_FACE('',(#771),#533,.F.);
#5486=ADVANCED_FACE('',(#772),#534,.F.);
#5487=ADVANCED_FACE('',(#773),#535,.F.);
#5488=ADVANCED_FACE('',(#774),#536,.F.);
#5489=ADVANCED_FACE('',(#775),#537,.F.);
#5490=ADVANCED_FACE('',(#776),#538,.F.);
#5705=CLOSED_SHELL('',(#5474,#5475,#5476,#5477,#5478,#5479,#5480,#5481,
#5482));
#5706=CLOSED_SHELL('',(#5483,#5484,#5485,#5486,#5487,#5488,#5489,#5490));
#6244=AXIS2_PLACEMENT_3D('',#9179,#7341,#7342);
#6245=AXIS2_PLACEMENT_3D('',#9180,#7343,#7344);
#6246=AXIS2_PLACEMENT_3D('',#9182,#7345,#7346);
#6247=AXIS2_PLACEMENT_3D('',#9183,#7347,#7348);
#6248=AXIS2_PLACEMENT_3D('',#9185,#7349,#7350);
#6249=AXIS2_PLACEMENT_3D('',#9187,#7352,#7353);
#6250=AXIS2_PLACEMENT_3D('',#9189,#7354,#7355);
#6251=AXIS2_PLACEMENT_3D('',#9191,#7357,#7358);
#6252=AXIS2_PLACEMENT_3D('',#9193,#7359,#7360);
#6253=AXIS2_PLACEMENT_3D('',#9195,#7362,#7363);
#6254=AXIS2_PLACEMENT_3D('',#9197,#7364,#7365);
#6255=AXIS2_PLACEMENT_3D('',#9198,#7366,#7367);
#6256=AXIS2_PLACEMENT_3D('',#9200,#7368,#7369);
#6257=AXIS2_PLACEMENT_3D('',#9202,#7371,#7372);
#6258=AXIS2_PLACEMENT_3D('',#9204,#7373,#7374);
#6259=AXIS2_PLACEMENT_3D('',#9206,#7376,#7377);
#6260=AXIS2_PLACEMENT_3D('',#9208,#7378,#7379);
#6261=AXIS2_PLACEMENT_3D('',#9210,#7381,#7382);
#6262=AXIS2_PLACEMENT_3D('',#9211,#7383,#7384);
#6263=AXIS2_PLACEMENT_3D('',#9220,#7389,#7390);
#6264=AXIS2_PLACEMENT_3D('',#9226,#7394,#7395);
#6265=AXIS2_PLACEMENT_3D('',#9232,#7399,#7400);
#6266=AXIS2_PLACEMENT_3D('',#9238,#7404,#7405);
#6267=AXIS2_PLACEMENT_3D('',#9244,#7409,#7410);
#6268=AXIS2_PLACEMENT_3D('',#9247,#7413,#7414);
#6269=AXIS2_PLACEMENT_3D('',#9248,#7415,#7416);
#7341=DIRECTION('axis',(0.,0.,1.));
#7342=DIRECTION('refdir',(1.,0.,0.));
#7343=DIRECTION('center_axis',(0.,1.,0.));
#7344=DIRECTION('ref_axis',(0.,0.,1.));
#7345=DIRECTION('center_axis',(0.,-1.,0.));
#7346=DIRECTION('ref_axis',(1.,0.,0.));
#7347=DIRECTION('center_axis',(0.,-1.,0.));
#7348=DIRECTION('ref_axis',(1.,0.,0.));
#7349=DIRECTION('center_axis',(0.,-1.,0.));
#7350=DIRECTION('ref_axis',(1.,0.,0.));
#7351=DIRECTION('',(0.707106781186548,0.707106781186547,8.65956056235493E-17));
#7352=DIRECTION('center_axis',(0.,-1.,0.));
#7353=DIRECTION('ref_axis',(1.,0.,0.));
#7354=DIRECTION('center_axis',(0.,-1.,0.));
#7355=DIRECTION('ref_axis',(1.,0.,0.));
#7356=DIRECTION('',(0.,1.,0.));
#7357=DIRECTION('center_axis',(0.,1.,0.));
#7358=DIRECTION('ref_axis',(1.,0.,0.));
#7359=DIRECTION('center_axis',(0.,-1.,0.));
#7360=DIRECTION('ref_axis',(1.,0.,0.));
#7361=DIRECTION('',(-0.707106781186547,0.707106781186548,-8.65956056235493E-17));
#7362=DIRECTION('center_axis',(0.,-1.,0.));
#7363=DIRECTION('ref_axis',(0.,0.,-1.));
#7364=DIRECTION('center_axis',(0.,-1.,0.));
#7365=DIRECTION('ref_axis',(1.,0.,0.));
#7366=DIRECTION('center_axis',(0.,1.,0.));
#7367=DIRECTION('ref_axis',(1.,0.,0.));
#7368=DIRECTION('center_axis',(0.,1.,0.));
#7369=DIRECTION('ref_axis',(1.,0.,0.));
#7370=DIRECTION('',(-0.447213595499958,0.894427190999916,-5.47678698264203E-17));
#7371=DIRECTION('center_axis',(0.,-1.,0.));
#7372=DIRECTION('ref_axis',(1.,0.,0.));
#7373=DIRECTION('center_axis',(0.,1.,0.));
#7374=DIRECTION('ref_axis',(1.,0.,0.));
#7375=DIRECTION('',(0.,1.,0.));
#7376=DIRECTION('center_axis',(0.,1.,0.));
#7377=DIRECTION('ref_axis',(1.,0.,0.));
#7378=DIRECTION('center_axis',(0.,-1.,0.));
#7379=DIRECTION('ref_axis',(1.,0.,0.));
#7380=DIRECTION('',(-0.707106781186547,0.707106781186548,-8.65956056235493E-17));
#7381=DIRECTION('center_axis',(0.,-1.,0.));
#7382=DIRECTION('ref_axis',(0.,0.,-1.));
#7383=DIRECTION('center_axis',(0.866025403784439,0.,-0.5));
#7384=DIRECTION('ref_axis',(0.5,0.,0.866025403784439));
#7385=DIRECTION('',(-0.5,0.,-0.866025403784439));
#7386=DIRECTION('',(0.,-1.,0.));
#7387=DIRECTION('',(0.5,0.,0.866025403784439));
#7388=DIRECTION('',(0.,-1.,0.));
#7389=DIRECTION('center_axis',(1.20185167898973E-16,0.,-1.));
#7390=DIRECTION('ref_axis',(1.,0.,1.20185167898973E-16));
#7391=DIRECTION('',(-1.,0.,-1.20185167898973E-16));
#7392=DIRECTION('',(0.,-1.,0.));
#7393=DIRECTION('',(1.,0.,1.20185167898973E-16));
#7394=DIRECTION('center_axis',(-0.866025403784439,0.,-0.5));
#7395=DIRECTION('ref_axis',(0.5,0.,-0.866025403784439));
#7396=DIRECTION('',(-0.5,0.,0.866025403784439));
#7397=DIRECTION('',(0.,-1.,0.));
#7398=DIRECTION('',(0.5,0.,-0.866025403784439));
#7399=DIRECTION('center_axis',(-0.866025403784439,0.,0.5));
#7400=DIRECTION('ref_axis',(-0.5,0.,-0.866025403784439));
#7401=DIRECTION('',(0.5,0.,0.866025403784439));
#7402=DIRECTION('',(0.,-1.,0.));
#7403=DIRECTION('',(-0.5,0.,-0.866025403784439));
#7404=DIRECTION('center_axis',(-2.40370335797945E-16,0.,1.));
#7405=DIRECTION('ref_axis',(-1.,0.,-2.40370335797945E-16));
#7406=DIRECTION('',(1.,0.,2.40370335797945E-16));
#7407=DIRECTION('',(0.,-1.,0.));
#7408=DIRECTION('',(-1.,0.,-2.40370335797945E-16));
#7409=DIRECTION('center_axis',(0.866025403784439,0.,0.5));
#7410=DIRECTION('ref_axis',(-0.5,0.,0.866025403784439));
#7411=DIRECTION('',(0.5,0.,-0.866025403784439));
#7412=DIRECTION('',(-0.5,0.,0.866025403784439));
#7413=DIRECTION('center_axis',(0.,1.,0.));
#7414=DIRECTION('ref_axis',(1.,0.,0.));
#7415=DIRECTION('center_axis',(0.,-1.,0.));
#7416=DIRECTION('ref_axis',(0.,0.,-1.));
#9179=CARTESIAN_POINT('',(0.,0.,0.));
#9180=CARTESIAN_POINT('Origin',(0.375,0.5,0.));
#9181=CARTESIAN_POINT('',(-0.375,0.5,-4.59242549680257E-17));
#9182=CARTESIAN_POINT('Origin',(0.,0.5,0.));
#9183=CARTESIAN_POINT('Origin',(0.,0.475,0.));
#9184=CARTESIAN_POINT('',(-0.425,0.45,-5.20474889637625E-17));
#9185=CARTESIAN_POINT('Origin',(0.,0.45,0.));
#9186=CARTESIAN_POINT('',(-0.4,0.475,-4.89858719658941E-17));
#9187=CARTESIAN_POINT('Origin',(0.,0.24,0.));
#9188=CARTESIAN_POINT('',(-0.425,0.0299999999999998,-5.20474889637625E-17));
#9189=CARTESIAN_POINT('Origin',(0.,0.0299999999999998,0.));
#9190=CARTESIAN_POINT('',(-0.425,0.24,-5.20474889637625E-17));
#9191=CARTESIAN_POINT('Origin',(0.,0.0150000000000001,0.));
#9192=CARTESIAN_POINT('',(-0.395,4.85722573273506E-17,-4.83735485663204E-17));
#9193=CARTESIAN_POINT('Origin',(0.,0.,0.));
#9194=CARTESIAN_POINT('',(-0.41,0.0150000000000001,-5.02105187650415E-17));
#9195=CARTESIAN_POINT('Origin',(0.27,0.,0.));
#9196=CARTESIAN_POINT('',(-0.27,0.,-3.30654635769785E-17));
#9197=CARTESIAN_POINT('Origin',(0.,0.,0.));
#9198=CARTESIAN_POINT('Origin',(0.,-0.02,0.));
#9199=CARTESIAN_POINT('',(-0.24505,-0.0498999999999999,3.00099698131059E-17));
#9200=CARTESIAN_POINT('Origin',(0.,-0.0498999999999999,0.));
#9201=CARTESIAN_POINT('',(-0.26,-0.02,-3.18408167778312E-17));
#9202=CARTESIAN_POINT('Origin',(0.,-0.995,0.));
#9203=CARTESIAN_POINT('',(-0.24505,-1.95495,3.00099698131059E-17));
#9204=CARTESIAN_POINT('Origin',(0.,-1.95495,0.));
#9205=CARTESIAN_POINT('',(-0.24505,-0.995,-3.00099698131059E-17));
#9206=CARTESIAN_POINT('Origin',(0.,-1.975,0.));
#9207=CARTESIAN_POINT('',(-0.2,-2.,-2.44929359829471E-17));
#9208=CARTESIAN_POINT('Origin',(0.,-2.,0.));
#9209=CARTESIAN_POINT('',(-0.225,-1.975,-2.75545529808154E-17));
#9210=CARTESIAN_POINT('Origin',(0.,-2.,0.));
#9211=CARTESIAN_POINT('Origin',(0.115470053837925,-0.5,-0.2));
#9212=CARTESIAN_POINT('',(0.23094010767585,-0.5,0.));
#9213=CARTESIAN_POINT('',(0.115470053837925,-0.5,-0.2));
#9214=CARTESIAN_POINT('',(0.23094010767585,-0.5,0.));
#9215=CARTESIAN_POINT('',(0.115470053837925,-0.8,-0.2));
#9216=CARTESIAN_POINT('',(0.115470053837925,-0.5,-0.2));
#9217=CARTESIAN_POINT('',(0.23094010767585,-0.8,0.));
#9218=CARTESIAN_POINT('',(0.23094010767585,-0.8,0.));
#9219=CARTESIAN_POINT('',(0.23094010767585,-0.5,0.));
#9220=CARTESIAN_POINT('Origin',(-0.115470053837925,-0.5,-0.2));
#9221=CARTESIAN_POINT('',(-0.115470053837925,-0.5,-0.2));
#9222=CARTESIAN_POINT('',(0.115470053837925,-0.5,-0.2));
#9223=CARTESIAN_POINT('',(-0.115470053837925,-0.8,-0.2));
#9224=CARTESIAN_POINT('',(-0.115470053837925,-0.5,-0.2));
#9225=CARTESIAN_POINT('',(0.115470053837925,-0.8,-0.2));
#9226=CARTESIAN_POINT('Origin',(-0.23094010767585,-0.5,-2.77555756156289E-17));
#9227=CARTESIAN_POINT('',(-0.23094010767585,-0.5,-2.82820063659975E-17));
#9228=CARTESIAN_POINT('',(-0.115470053837925,-0.5,-0.2));
#9229=CARTESIAN_POINT('',(-0.23094010767585,-0.8,-2.77555756156289E-17));
#9230=CARTESIAN_POINT('',(-0.23094010767585,-0.5,-2.82820063659975E-17));
#9231=CARTESIAN_POINT('',(-0.115470053837925,-0.8,-0.2));
#9232=CARTESIAN_POINT('Origin',(-0.115470053837925,-0.5,0.2));
#9233=CARTESIAN_POINT('',(-0.115470053837925,-0.5,0.2));
#9234=CARTESIAN_POINT('',(-0.23094010767585,-0.5,-2.82820063659975E-17));
#9235=CARTESIAN_POINT('',(-0.115470053837925,-0.8,0.2));
#9236=CARTESIAN_POINT('',(-0.115470053837925,-0.5,0.2));
#9237=CARTESIAN_POINT('',(-0.23094010767585,-0.8,-2.82820063659975E-17));
#9238=CARTESIAN_POINT('Origin',(0.115470053837925,-0.5,0.2));
#9239=CARTESIAN_POINT('',(0.115470053837925,-0.5,0.2));
#9240=CARTESIAN_POINT('',(-0.115470053837925,-0.5,0.2));
#9241=CARTESIAN_POINT('',(0.115470053837925,-0.8,0.2));
#9242=CARTESIAN_POINT('',(0.115470053837925,-0.5,0.2));
#9243=CARTESIAN_POINT('',(-0.115470053837925,-0.8,0.2));
#9244=CARTESIAN_POINT('Origin',(0.23094010767585,-0.5,0.));
#9245=CARTESIAN_POINT('',(0.115470053837925,-0.5,0.2));
#9246=CARTESIAN_POINT('',(0.115470053837925,-0.8,0.2));
#9247=CARTESIAN_POINT('Origin',(0.,-0.5,0.));
#9248=CARTESIAN_POINT('Origin',(0.,-0.8,0.));
#10904=UNCERTAINTY_MEASURE_WITH_UNIT(LENGTH_MEASURE(0.001),#10958,
'DISTANCE_ACCURACY_VALUE',
'Maximum model space distance between geometric entities at asserted c
onnectivities');
#10926=UNCERTAINTY_MEASURE_WITH_UNIT(LENGTH_MEASURE(0.001),#10958,
'DISTANCE_ACCURACY_VALUE',
'Maximum model space distance between geometric entities at asserted c
onnectivities');
#10935=(
GEOMETRIC_REPRESENTATION_CONTEXT(3)
GLOBAL_UNCERTAINTY_ASSIGNED_CONTEXT((#10904))
GLOBAL_UNIT_ASSIGNED_CONTEXT((#10958,#10960,#10961))
REPRESENTATION_CONTEXT('','3D')
);
#10957=(
GEOMETRIC_REPRESENTATION_CONTEXT(3)
GLOBAL_UNCERTAINTY_ASSIGNED_CONTEXT((#10926))
GLOBAL_UNIT_ASSIGNED_CONTEXT((#10958,#10960,#10961))
REPRESENTATION_CONTEXT('','3D')
);
#10958=(
LENGTH_UNIT()
NAMED_UNIT(*)
SI_UNIT(.CENTI.,.METRE.)
);
#10960=(
NAMED_UNIT(*)
PLANE_ANGLE_UNIT()
SI_UNIT($,.RADIAN.)
);
#10961=(
NAMED_UNIT(*)
SI_UNIT($,.STERADIAN.)
SOLID_ANGLE_UNIT()
);
#10970=SHAPE_DEFINITION_REPRESENTATION(#11000,#11072);
#11000=PRODUCT_DEFINITION_SHAPE('',$,#11103);
#11072=SHAPE_REPRESENTATION('',(#6244),#10935);
#11094=PRODUCT_DEFINITION_CONTEXT('part definition',#11186,'design');
#11103=PRODUCT_DEFINITION('Cap Screw - M5x20','Cap Screw - M5x20',#11133,
#11094);
#11133=PRODUCT_DEFINITION_FORMATION('',$,#11196);
#11186=APPLICATION_CONTEXT(
'Core Data for Automotive Mechanical Design Process');
#11187=PRODUCT_CONTEXT('part definition',#11186,'mechanical');
#11196=PRODUCT('Cap Screw - M5x20','Cap Screw - M5x20',
'Cap Screw - M5x20',(#11187));
#11288=COLOUR_RGB('Black',0.12,0.14,0.17);
#11289=FILL_AREA_STYLE_COLOUR('',#11288);
#11290=FILL_AREA_STYLE('',(#11289));
#11291=SURFACE_STYLE_FILL_AREA(#11290);
#11292=SURFACE_SIDE_STYLE('',(#11291));
#11293=SURFACE_STYLE_USAGE(.BOTH.,#11292);
#11294=PRESENTATION_STYLE_ASSIGNMENT((#11293));
ENDSEC;
END-ISO-10303-21;
